ISO-10303-21;
HEADER;
FILE_DESCRIPTION (('STEP AP214'),
    '1' );
FILE_NAME ('Nut.step',
    '2026-10-06T08:09:25',
    ( '' ),
    ( '' ),
    'SwSTEP 2.0',
    'SolidWorks 2021',
    '' );
FILE_SCHEMA (( 'AUTOMOTIVE_DESIGN' ));
ENDSEC;

DATA;
#86=DIRECTION ( 'NONE',  ( 8.438582421954109416E-32, 0.000000000000000000, 1.000000000000000000 ) ) ;
#88=ORIENTED_EDGE ( 'NONE', *, *, #2993, .T. ) ;
#107=AXIS2_PLACEMENT_3D ( 'NONE', #10783, #22922, #6797 ) ;
#163=CARTESIAN_POINT ( 'NONE',  ( 4.346882592290810088, -1.739972214219157598, -1.970978495615625325 ) ) ;
#171=ORIENTED_EDGE ( 'NONE', *, *, #19907, .F. ) ;
#172=VERTEX_POINT ( 'NONE', #11900 ) ;
#226=VERTEX_POINT ( 'NONE', #7205 ) ;
#245=PRODUCT_CONTEXT ( 'NONE', #18364, 'mechanical' ) ;
#281=CARTESIAN_POINT ( 'NONE',  ( 5.484827557301438894, 1.325747111984056037, 0.000000000000000000 ) ) ;
#308=ADVANCED_FACE ( 'NONE', ( #18028 ), #17460, .T. ) ;
#323=FACE_OUTER_BOUND ( 'NONE', #12620, .T. ) ;
#341=CIRCLE ( 'NONE', #13120, 4.750000000000000000 ) ;
#384=CARTESIAN_POINT ( 'NONE',  ( 2.966164998648776141, 1.454929939081825330, -4.362451518707862519 ) ) ;
#410=CARTESIAN_POINT ( 'NONE',  ( 2.742413778650726108, -1.325747111984059590, 4.749999999999997335 ) ) ;
#446=ADVANCED_FACE ( 'NONE', ( #19058 ), #22478, .F. ) ;
#456=EDGE_CURVE ( 'NONE', #6638, #13441, #21115, .T. ) ;
#483=B_SPLINE_CURVE_WITH_KNOTS ( 'NONE', 3,
 ( #1623, #3166, #6801, #10448 ),
 .UNSPECIFIED., .F., .F.,
 ( 4, 4 ),
 ( 2.380735702043574917E-07, 0.002775112046897004661 ),
 .UNSPECIFIED. ) ;
#533=CARTESIAN_POINT ( 'NONE',  ( 1.849731447979668930, 1.560358803171613351, -4.750000000000025757 ) ) ;
#564=CARTESIAN_POINT ( 'NONE',  ( 5.484827557301438894, 1.325747111984056037, 0.000000000000000000 ) ) ;
#566=CARTESIAN_POINT ( 'NONE',  ( -5.484827557301438894, 1.325747111984031834, 0.000000000000000000 ) ) ;
#580=CIRCLE ( 'NONE', #8078, 2.500000000000000000 ) ;
#646=ADVANCED_FACE ( 'NONE', ( #16203 ), #19002, .T. ) ;
#707=CARTESIAN_POINT ( 'NONE',  ( 0.000000000000000000, -1.750000000000001554, 0.000000000000000000 ) ) ;
#719=ORIENTED_EDGE ( 'NONE', *, *, #19907, .T. ) ;
#829=EDGE_LOOP ( 'NONE', ( #9472, #14648, #21204, #1235, #22182, #6330 ) ) ;
#835=ORIENTED_EDGE ( 'NONE', *, *, #15747, .T. ) ;
#841=CARTESIAN_POINT ( 'NONE',  ( 0.000000000000000000, -1.750000000000001554, 0.000000000000000000 ) ) ;
#880=CARTESIAN_POINT ( 'NONE',  ( -2.742413778650615086, 1.325747111984059590, -4.750000000000000888 ) ) ;
#931=ADVANCED_FACE ( 'NONE', ( #11380 ), #9509, .F. ) ;
#976=AXIS2_PLACEMENT_3D ( 'NONE', #9197, #14370, #1677 ) ;
#1048=AXIS2_PLACEMENT_3D ( 'NONE', #19388, #3733, #18095 ) ;
#1084=CARTESIAN_POINT ( 'NONE',  ( -2.742413778650712342, 1.749999999999973799, 4.749999999999999112 ) ) ;
#1139=CARTESIAN_POINT ( 'NONE',  ( 0.000000000000000000, 1.750000000000001554, 0.000000000000000000 ) ) ;
#1179=ORIENTED_EDGE ( 'NONE', *, *, #1875, .F. ) ;
#1184=EDGE_CURVE ( 'NONE', #16673, #23235, #22737, .T. ) ;
#1186=CARTESIAN_POINT ( 'NONE',  ( -2.742413778650615086, 1.325747111984059590, -4.750000000000000888 ) ) ;
#1199=EDGE_CURVE ( 'NONE', #1642, #6272, #16255, .T. ) ;
#1209=EDGE_LOOP ( 'NONE', ( #6411, #6701, #20193 ) ) ;
#1235=ORIENTED_EDGE ( 'NONE', *, *, #20428, .F. ) ;
#1251=CYLINDRICAL_SURFACE ( 'NONE', #10241, 2.500000000000000000 ) ;
#1312=CARTESIAN_POINT ( 'NONE',  ( -0.4634555469063579292, 1.750000000000002220, 4.749999999999999112 ) ) ;
#1323=CONICAL_SURFACE ( 'NONE', #16330, 4.750000000000000888, 1.047197551196600074 ) ;
#1327=ORIENTED_EDGE ( 'NONE', *, *, #19749, .F. ) ;
#1372=CARTESIAN_POINT ( 'NONE',  ( -0.9238745061264534986, -1.710161125106381963, 4.749999999999999112 ) ) ;
#1387=CARTESIAN_POINT ( 'NONE',  ( 0.4637351970278817959, 1.750000000000001776, 4.749999999999999112 ) ) ;
#1435=ORIENTED_EDGE ( 'NONE', *, *, #20235, .F. ) ;
#1439=LINE ( 'NONE', #21221, #3812 ) ;
#1449=CARTESIAN_POINT ( 'NONE',  ( 4.113620667976075396, -1.749999999999998002, -2.375000000000002220 ) ) ;
#1450=CARTESIAN_POINT ( 'NONE',  ( 5.261076337303417283, 1.454929939081818002, 0.3875484812921120015 ) ) ;
#1472=( GEOMETRIC_REPRESENTATION_CONTEXT ( 3 ) GLOBAL_UNCERTAINTY_ASSIGNED_CONTEXT ( ( #3709 ) ) GLOBAL_UNIT_ASSIGNED_CONTEXT ( ( #13921, #3112, #6999 ) ) REPRESENTATION_CONTEXT ( 'NONE', 'WORKASPACE' ) );
#1594=CARTESIAN_POINT ( 'NONE',  ( 3.646393709166112718, 1.750000000000001998, 3.184260831324768226 ) ) ;
#1622=ADVANCED_FACE ( 'NONE', ( #19551 ), #8105, .T. ) ;
#1623=CARTESIAN_POINT ( 'NONE',  ( -5.484827557301438894, -1.325747111984083793, 0.000000000000000000 ) ) ;
#1633=AXIS2_PLACEMENT_3D ( 'NONE', #19620, #5400, #15962 ) ;
#1639=CIRCLE ( 'NONE', #2014, 2.500000000000000000 ) ;
#1642=VERTEX_POINT ( 'NONE', #5793 ) ;
#1677=DIRECTION ( 'NONE',  ( -8.438582421954109416E-32, 0.000000000000000000, -1.000000000000000000 ) ) ;
#1695=ORIENTED_EDGE ( 'NONE', *, *, #16541, .T. ) ;
#1735=DIRECTION ( 'NONE',  ( 0.000000000000000000, -1.000000000000000000, 0.000000000000000000 ) ) ;
#1740=CARTESIAN_POINT ( 'NONE',  ( 3.061616997868385113E-16, -1.750000000000001554, 2.500000000000000000 ) ) ;
#1748=CARTESIAN_POINT ( 'NONE',  ( -3.534277608971974516, -1.672424706883812062, -3.378451613207310356 ) ) ;
#1761=FACE_BOUND ( 'NONE', #21416, .T. ) ;
#1779=EDGE_CURVE ( 'NONE', #21726, #16673, #7567, .T. ) ;
#1796=CARTESIAN_POINT ( 'NONE',  ( 4.229990831856818900, 1.750000000000002442, 2.173440963673456405 ) ) ;
#1837=CARTESIAN_POINT ( 'NONE',  ( 1.849731447993483435, 1.560358803165483366, 4.749999999999998224 ) ) ;
#1838=CARTESIAN_POINT ( 'NONE',  ( 2.298974087845762959, -1.453757124411863222, 4.749999999999999112 ) ) ;
#1861=CARTESIAN_POINT ( 'NONE',  ( -3.191035955565411975, 1.584759246591057824, -3.972963596181423362 ) ) ;
#1875=EDGE_CURVE ( 'NONE', #5138, #4916, #11230, .T. ) ;
#1878=EDGE_CURVE ( 'NONE', #226, #5138, #15683, .T. ) ;
#1899=DIRECTION ( 'NONE',  ( 0.000000000000000000, -1.000000000000000000, 0.000000000000000000 ) ) ;
#1900=CARTESIAN_POINT ( 'NONE',  ( 5.261076337303422612, -1.454929939081816226, -0.3875484812921113353 ) ) ;
#1991=AXIS2_PLACEMENT_3D ( 'NONE', #16077, #10680, #21636 ) ;
#2014=AXIS2_PLACEMENT_3D ( 'NONE', #21294, #11269, #13039 ) ;
#2050=EDGE_CURVE ( 'NONE', #18266, #6638, #12897, .T. ) ;
#2063=VECTOR ( 'NONE', #18810, 1000.000000000000000 ) ;
#2065=ORIENTED_EDGE ( 'NONE', *, *, #2784, .F. ) ;
#2101=DIRECTION ( 'NONE',  ( 0.000000000000000000, -1.000000000000000000, 0.000000000000000000 ) ) ;
#2210=ORIENTED_EDGE ( 'NONE', *, *, #19749, .T. ) ;
#2211=AXIS2_PLACEMENT_3D ( 'NONE', #21190, #11761, #2833 ) ;
#2352=EDGE_LOOP ( 'NONE', ( #3577, #13267, #15281, #21360, #3708, #9622 ) ) ;
#2380=EDGE_LOOP ( 'NONE', ( #13614, #88, #18770 ) ) ;
#2385=B_SPLINE_CURVE_WITH_KNOTS ( 'NONE', 3,
 ( #23157, #6918, #3158, #5267 ),
 .UNSPECIFIED., .F., .F.,
 ( 4, 4 ),
 ( 2.380735702043749618E-07, 0.002775112046897000757 ),
 .UNSPECIFIED. ) ;
#2401=CARTESIAN_POINT ( 'NONE',  ( 4.113620667976075396, -1.749999999999998002, -2.375000000000002220 ) ) ;
#2471=CARTESIAN_POINT ( 'NONE',  ( 0.9337610948747031570, -1.709055945004938293, -4.750000000000025757 ) ) ;
#2516=DIRECTION ( 'NONE',  ( -8.438582421954109416E-32, 0.000000000000000000, -1.000000000000000000 ) ) ;
#2670=CONICAL_SURFACE ( 'NONE', #3064, 4.750000000000000000, 1.047197551196600074 ) ;
#2692=DIRECTION ( 'NONE',  ( 1.000000000000000000, 0.000000000000000000, 1.581383788144386089E-16 ) ) ;
#2784=EDGE_CURVE ( 'NONE', #13233, #18266, #3011, .T. ) ;
#2790=CARTESIAN_POINT ( 'NONE',  ( -4.113620667976075396, -1.750000000000001554, 2.374999999999986677 ) ) ;
#2795=CIRCLE ( 'NONE', #21962, 4.750000000000000000 ) ;
#2814=AXIS2_PLACEMENT_3D ( 'NONE', #12701, #8594, #15760 ) ;
#2830=CARTESIAN_POINT ( 'NONE',  ( 0.000000000000000000, 1.750000000000001554, 0.000000000000000000 ) ) ;
#2833=DIRECTION ( 'NONE',  ( 8.438582421954109416E-32, 0.000000000000000000, 1.000000000000000000 ) ) ;
#2868=CARTESIAN_POINT ( 'NONE',  ( 0.000000000000000000, -1.750000000000001554, 0.000000000000000000 ) ) ;
#2904=EDGE_LOOP ( 'NONE', ( #17821, #20769, #8065 ) ) ;
#2953=CARTESIAN_POINT ( 'NONE',  ( -2.296348136192898792, 1.454515171358711889, 4.749999999999999112 ) ) ;
#2963=DIRECTION ( 'NONE',  ( 0.000000000000000000, 0.000000000000000000, 1.000000000000000000 ) ) ;
#2993=EDGE_CURVE ( 'NONE', #16467, #16377, #3582, .T. ) ;
#3011=LINE ( 'NONE', #12518, #21744 ) ;
#3025=ADVANCED_BREP_SHAPE_REPRESENTATION ( '', ( #5146, #22115 ), #18753 ) ;
#3049=PLANE ( 'NONE',  #5194 ) ;
#3064=AXIS2_PLACEMENT_3D ( 'NONE', #5503, #16413, #12662 ) ;
#3090=CARTESIAN_POINT ( 'NONE',  ( 0.000000000000000000, -1.750000000000001554, 0.000000000000000000 ) ) ;
#3105=FACE_OUTER_BOUND ( 'NONE', #9826, .T. ) ;
#3112=( NAMED_UNIT ( * ) PLANE_ANGLE_UNIT ( ) SI_UNIT ( $, .RADIAN. ) );
#3148=B_SPLINE_CURVE_WITH_KNOTS ( 'NONE', 3,
 ( #17916, #8977, #16477, #18034, #14610, #18256, #384, #12730 ),
 .UNSPECIFIED., .F., .F.,
 ( 4, 2, 2, 4 ),
 ( 0.002775112046897006395, 0.003466237704215411296, 0.004157363361533816630, 0.005539614676170626431 ),
 .UNSPECIFIED. ) ;
#3158=CARTESIAN_POINT ( 'NONE',  ( -3.646393709166105168, -1.750000000000010214, 3.184260831324758456 ) ) ;
#3166=CARTESIAN_POINT ( 'NONE',  ( -5.036205380386573616, -1.584759246591067594, -0.7770364038185282318 ) ) ;
#3173=DIRECTION ( 'NONE',  ( -1.581383788144386089E-16, 0.000000000000000000, 1.000000000000000000 ) ) ;
#3190=CARTESIAN_POINT ( 'NONE',  ( 2.742413778650726108, -1.325747111984059590, 4.749999999999997335 ) ) ;
#3203=EDGE_LOOP ( 'NONE', ( #22259, #4579, #1179 ) ) ;
#3204=AXIS2_PLACEMENT_3D ( 'NONE', #6832, #3539, #8946 ) ;
#3235=SURFACE_STYLE_USAGE ( .BOTH. , #14389 ) ;
#3402=PLANE ( 'NONE',  #15141 ) ;
#3539=DIRECTION ( 'NONE',  ( -0.000000000000000000, 1.000000000000000000, 0.000000000000000000 ) ) ;
#3558=CARTESIAN_POINT ( 'NONE',  ( -4.113620667976089607, -1.750000000000001554, -2.375000000000005773 ) ) ;
#3577=ORIENTED_EDGE ( 'NONE', *, *, #1199, .F. ) ;
#3582=B_SPLINE_CURVE_WITH_KNOTS ( 'NONE', 3,
 ( #21825, #12995, #533, #14641, #9584, #20172 ),
 .UNSPECIFIED., .F., .F.,
 ( 4, 2, 4 ),
 ( 0.001997790247439712105, 0.003382245507025886423, 0.004766700766612060741 ),
 .UNSPECIFIED. ) ;
#3596=CARTESIAN_POINT ( 'NONE',  ( 3.061616997868385113E-16, 1.750000000000001554, 2.500000000000000000 ) ) ;
#3639=CARTESIAN_POINT ( 'NONE',  ( -2.742413778650615086, 1.325747111984059590, -4.750000000000000888 ) ) ;
#3708=ORIENTED_EDGE ( 'NONE', *, *, #19543, .F. ) ;
#3709=UNCERTAINTY_MEASURE_WITH_UNIT (LENGTH_MEASURE( 1.000000000000000082E-05 ), #13921, 'distance_accuracy_value', 'NONE');
#3733=DIRECTION ( 'NONE',  ( -0.8660254037844385966, -7.888609052210117178E-31, -0.5000000000000001110 ) ) ;
#3763=VERTEX_POINT ( 'NONE', #564 ) ;
#3795=ORIENTED_EDGE ( 'NONE', *, *, #20235, .T. ) ;
#3812=VECTOR ( 'NONE', #13907, 1000.000000000000000 ) ;
#3857=DIRECTION ( 'NONE',  ( 0.5000000000000000000, 0.000000000000000000, -0.8660254037844385966 ) ) ;
#3913=VERTEX_POINT ( 'NONE', #21017 ) ;
#3934=CARTESIAN_POINT ( 'NONE',  ( 4.113620667976089607, 1.749999999999973799, 2.375000000000000444 ) ) ;
#4101=DIRECTION ( 'NONE',  ( 0.000000000000000000, 1.000000000000000000, 0.000000000000000000 ) ) ;
#4115=DIRECTION ( 'NONE',  ( 8.438582421954109416E-32, 0.000000000000000000, 1.000000000000000000 ) ) ;
#4122=CARTESIAN_POINT ( 'NONE',  ( 0.000000000000000000, 1.750000000000001554, 0.000000000000000000 ) ) ;
#4160=ORIENTED_EDGE ( 'NONE', *, *, #2993, .F. ) ;
#4197=ADVANCED_FACE ( 'NONE', ( #22753 ), #18327, .T. ) ;
#4216=B_SPLINE_CURVE_WITH_KNOTS ( 'NONE', 3,
 ( #17892, #19775, #10821, #14245, #7312, #10924, #18012, #14351 ),
 .UNSPECIFIED., .F., .F.,
 ( 4, 2, 2, 4 ),
 ( 0.002775112046897009431, 0.003466237704215413898, 0.004157363361533818365, 0.005539614676170626431 ),
 .UNSPECIFIED. ) ;
#4285=ADVANCED_FACE ( 'NONE', ( #3105 ), #4407, .T. ) ;
#4317=FACE_OUTER_BOUND ( 'NONE', #7342, .T. ) ;
#4332=EDGE_CURVE ( 'NONE', #5138, #3763, #11137, .T. ) ;
#4407=CONICAL_SURFACE ( 'NONE', #4807, 4.750000000000000000, 1.047197551196600074 ) ;
#4428=B_SPLINE_CURVE_WITH_KNOTS ( 'NONE', 3,
 ( #8050, #16967, #22403, #22520, #20878, #880 ),
 .UNSPECIFIED., .F., .F.,
 ( 4, 2, 4 ),
 ( 0.004766700766612060741, 0.006150321146734550118, 0.007533941526857039495 ),
 .UNSPECIFIED. ) ;
#4457=CONICAL_SURFACE ( 'NONE', #22900, 4.750000000000000888, 1.047197551196600074 ) ;
#4466=CARTESIAN_POINT ( 'NONE',  ( 2.742413778650823364, -1.325747111984059590, -4.750000000000000888 ) ) ;
#4513=DIRECTION ( 'NONE',  ( -8.438582421954109416E-32, 0.000000000000000000, -1.000000000000000000 ) ) ;
#4565=LINE ( 'NONE', #19268, #8493 ) ;
#4579=ORIENTED_EDGE ( 'NONE', *, *, #8393, .T. ) ;
#4655=VECTOR ( 'NONE', #1899, 1000.000000000000000 ) ;
#4709=CARTESIAN_POINT ( 'NONE',  ( 3.646393709166121599, -1.749999999999999556, -3.184260831324760233 ) ) ;
#4756=ADVANCED_FACE ( 'NONE', ( #22594 ), #7044, .F. ) ;
#4757=AXIS2_PLACEMENT_3D ( 'NONE', #15594, #6557, #13726 ) ;
#4781=ADVANCED_FACE ( 'NONE', ( #7381 ), #11107, .T. ) ;
#4807=AXIS2_PLACEMENT_3D ( 'NONE', #18754, #19099, #13576 ) ;
#4825=DIRECTION ( 'NONE',  ( 8.438582421954110511E-32, 0.000000000000000000, 1.000000000000000000 ) ) ;
#4890=ORIENTED_EDGE ( 'NONE', *, *, #2050, .T. ) ;
#4916=VERTEX_POINT ( 'NONE', #17858 ) ;
#4941=EDGE_CURVE ( 'NONE', #23235, #172, #18143, .T. ) ;
#4943=CARTESIAN_POINT ( 'NONE',  ( 0.000000000000000000, 0.000000000000000000, 0.000000000000000000 ) ) ;
#5025=CARTESIAN_POINT ( 'NONE',  ( -5.036205380386646446, 1.584759246591022297, 0.7770364038185694211 ) ) ;
#5071=B_SPLINE_CURVE_WITH_KNOTS ( 'NONE', 3,
 ( #9492, #14790, #7614, #18551, #18093, #21973, #16654, #566 ),
 .UNSPECIFIED., .F., .F.,
 ( 4, 2, 2, 4 ),
 ( 0.002775112046897002492, 0.003466237704215407826, 0.004157363361533813161, 0.005539614676170624696 ),
 .UNSPECIFIED. ) ;
#5108=VERTEX_POINT ( 'NONE', #3596 ) ;
#5138=VERTEX_POINT ( 'NONE', #3934 ) ;
#5146=MANIFOLD_SOLID_BREP ( 'Cut-Extrude2', #6935 ) ;
#5168=ORIENTED_EDGE ( 'NONE', *, *, #17211, .T. ) ;
#5170=CARTESIAN_POINT ( 'NONE',  ( -2.966164998648648687, -1.454929939081855750, -4.362451518707887388 ) ) ;
#5193=ORIENTED_EDGE ( 'NONE', *, *, #8046, .T. ) ;
#5194=AXIS2_PLACEMENT_3D ( 'NONE', #19161, #3173, #2692 ) ;
#5216=CARTESIAN_POINT ( 'NONE',  ( -2.109645605488527628E-31, 1.750000000000001554, -2.500000000000000000 ) ) ;
#5267=CARTESIAN_POINT ( 'NONE',  ( -4.113620667976075396, -1.750000000000001554, 2.374999999999986677 ) ) ;
#5306=DIRECTION ( 'NONE',  ( 1.000000000000000000, 0.000000000000000000, 0.000000000000000000 ) ) ;
#5329=CARTESIAN_POINT ( 'NONE',  ( 5.484827557301452217, -1.325747111984059590, 0.000000000000000000 ) ) ;
#5387=CARTESIAN_POINT ( 'NONE',  ( 0.9337610950194882298, 1.709055944985350850, 4.749999999999999112 ) ) ;
#5398=DIRECTION ( 'NONE',  ( 8.438582421954110511E-32, 0.000000000000000000, 1.000000000000000000 ) ) ;
#5400=DIRECTION ( 'NONE',  ( 0.000000000000000000, -1.000000000000000000, 0.000000000000000000 ) ) ;
#5416=CARTESIAN_POINT ( 'NONE',  ( -4.113620667976089607, -1.750000000000001554, -2.375000000000005773 ) ) ;
#5423=CARTESIAN_POINT ( 'NONE',  ( -1.839530896101882362, -1.562503694756887995, -4.750000000000026645 ) ) ;
#5437=EDGE_CURVE ( 'NONE', #17782, #7940, #6601, .T. ) ;
#5503=CARTESIAN_POINT ( 'NONE',  ( 0.000000000000000000, 1.750000000000001554, 0.000000000000000000 ) ) ;
#5515=PLANE ( 'NONE',  #1048 ) ;
#5601=SURFACE_SIDE_STYLE ('',( #23255 ) ) ;
#5624=DIRECTION ( 'NONE',  ( -8.438582421954109416E-32, 0.000000000000000000, -1.000000000000000000 ) ) ;
#5697=EDGE_LOOP ( 'NONE', ( #719, #12360 ) ) ;
#5793=CARTESIAN_POINT ( 'NONE',  ( -5.484827557301438894, 1.325747111984031834, 0.000000000000000000 ) ) ;
#6121=CIRCLE ( 'NONE', #20775, 4.750000000000000888 ) ;
#6254=DIRECTION ( 'NONE',  ( 0.000000000000000000, 1.000000000000000000, 0.000000000000000000 ) ) ;
#6272=VERTEX_POINT ( 'NONE', #16078 ) ;
#6305=EDGE_LOOP ( 'NONE', ( #9339, #2210, #835, #14254 ) ) ;
#6312=DIRECTION ( 'NONE',  ( -8.438582421954110511E-32, 0.000000000000000000, -1.000000000000000000 ) ) ;
#6317=CIRCLE ( 'NONE', #18331, 4.750000000000000888 ) ;
#6330=ORIENTED_EDGE ( 'NONE', *, *, #21348, .F. ) ;
#6370=CARTESIAN_POINT ( 'NONE',  ( 0.000000000000000000, 1.749999999999973799, 4.749999999999997335 ) ) ;
#6411=ORIENTED_EDGE ( 'NONE', *, *, #20428, .T. ) ;
#6448=EDGE_LOOP ( 'NONE', ( #20248, #15947, #20566, #15318, #7290, #11405 ) ) ;
#6522=DIRECTION ( 'NONE',  ( 0.000000000000000000, -1.000000000000000000, 0.000000000000000000 ) ) ;
#6557=DIRECTION ( 'NONE',  ( 0.000000000000000000, -1.000000000000000000, 0.000000000000000000 ) ) ;
#6572=ORIENTED_EDGE ( 'NONE', *, *, #21155, .T. ) ;
#6601=B_SPLINE_CURVE_WITH_KNOTS ( 'NONE', 3,
 ( #1449, #8623, #163, #18038, #8980, #19797, #1900, #5329 ),
 .UNSPECIFIED., .F., .F.,
 ( 4, 2, 2, 4 ),
 ( 0.002775112046896986880, 0.003466237704215396551, 0.004157363361533805354, 0.005539614676170624696 ),
 .UNSPECIFIED. ) ;
#6621=LINE ( 'NONE', #15557, #22713 ) ;
#6638=VERTEX_POINT ( 'NONE', #8865 ) ;
#6655=CARTESIAN_POINT ( 'NONE',  ( 0.000000000000000000, -1.750000000000025757, 4.749999999999973355 ) ) ;
#6680=CARTESIAN_POINT ( 'NONE',  ( 2.742413778650726108, 1.325747111984056037, 4.749999999999997335 ) ) ;
#6701=ORIENTED_EDGE ( 'NONE', *, *, #10902, .F. ) ;
#6751=FILL_AREA_STYLE ('',( #10742 ) ) ;
#6791=VECTOR ( 'NONE', #2101, 1000.000000000000000 ) ;
#6797=DIRECTION ( 'NONE',  ( -8.438582421954109416E-32, 0.000000000000000000, -1.000000000000000000 ) ) ;
#6800=DIRECTION ( 'NONE',  ( 8.438582421954110511E-32, 0.000000000000000000, -1.000000000000000000 ) ) ;
#6801=CARTESIAN_POINT ( 'NONE',  ( -4.580847626785981674, -1.750000000000056399, -1.565739168675184478 ) ) ;
#6829=CARTESIAN_POINT ( 'NONE',  ( 3.534277608972077545, -1.672424706883764989, 3.378451613207321014 ) ) ;
#6832=CARTESIAN_POINT ( 'NONE',  ( 0.000000000000000000, 1.750000000000001554, 0.000000000000000000 ) ) ;
#6873=SURFACE_STYLE_FILL_AREA ( #6751 ) ;
#6918=CARTESIAN_POINT ( 'NONE',  ( -3.191035955565509674, -1.584759246591024517, 3.972963596181419810 ) ) ;
#6935=CLOSED_SHELL ( 'NONE', ( #446, #4756, #22376, #15953, #7228, #931, #20064, #20071, #18879, #11164, #20097, #4781, #1622, #7752, #8694, #4197, #4285, #14995, #21613, #646, #18889, #308 ) ) ;
#6950=AXIS2_PLACEMENT_3D ( 'NONE', #841, #6254, #4825 ) ;
#6952=ORIENTED_EDGE ( 'NONE', *, *, #15265, .T. ) ;
#6999=( NAMED_UNIT ( * ) SI_UNIT ( $, .STERADIAN. ) SOLID_ANGLE_UNIT ( ) );
#7008=ORIENTED_EDGE ( 'NONE', *, *, #9157, .T. ) ;
#7044=PLANE ( 'NONE',  #17487 ) ;
#7074=AXIS2_PLACEMENT_3D ( 'NONE', #2868, #15088, #4513 ) ;
#7148=FACE_OUTER_BOUND ( 'NONE', #21148, .T. ) ;
#7156=CARTESIAN_POINT ( 'NONE',  ( 0.000000000000000000, 1.749999999999973799, 4.749999999999997335 ) ) ;
#7184=CARTESIAN_POINT ( 'NONE',  ( -2.742413778650615086, -1.325747111984059590, -4.749999999999997335 ) ) ;
#7201=EDGE_LOOP ( 'NONE', ( #22148, #6572, #171, #12864 ) ) ;
#7205=CARTESIAN_POINT ( 'NONE',  ( 0.000000000000000000, 1.749999999999973799, 4.749999999999997335 ) ) ;
#7228=ADVANCED_FACE ( 'NONE', ( #9997 ), #3049, .F. ) ;
#7290=ORIENTED_EDGE ( 'NONE', *, *, #18015, .F. ) ;
#7296=CARTESIAN_POINT ( 'NONE',  ( -3.191783008269798660, -1.561572887838416079, -3.971669662941494927 ) ) ;
#7312=CARTESIAN_POINT ( 'NONE',  ( -3.534277608972057561, 1.672424706883767875, 3.378451613207333448 ) ) ;
#7342=EDGE_LOOP ( 'NONE', ( #15452, #8494, #10513, #8894, #1435, #10833 ) ) ;
#7358=FILL_AREA_STYLE_COLOUR ( '', #13399 ) ;
#7381=FACE_OUTER_BOUND ( 'NONE', #18302, .T. ) ;
#7409=CARTESIAN_POINT ( 'NONE',  ( -2.296348136152779329, -1.454515171370276860, -4.750000000000026645 ) ) ;
#7567=B_SPLINE_CURVE_WITH_KNOTS ( 'NONE', 3,
 ( #15521, #8590, #13771, #15287, #6829, #18951, #22481, #3190 ),
 .UNSPECIFIED., .F., .F.,
 ( 4, 2, 2, 4 ),
 ( 0.002775112046897012467, 0.003466237704215415199, 0.004157363361533817497, 0.005539614676170622962 ),
 .UNSPECIFIED. ) ;
#7614=CARTESIAN_POINT ( 'NONE',  ( -4.346882592290722158, 1.739972214219213331, -1.970978495615576698 ) ) ;
#7617=PRODUCT_DEFINITION ( 'UNKNOWN', '', #21044, #20651 ) ;
#7633=DIRECTION ( 'NONE',  ( 0.5000000000000003331, 0.000000000000000000, 0.8660254037844384856 ) ) ;
#7644=CONICAL_SURFACE ( 'NONE', #18917, 4.750000000000000000, 1.047197551196600074 ) ;
#7692=VERTEX_POINT ( 'NONE', #2790 ) ;
#7723=B_SPLINE_CURVE_WITH_KNOTS ( 'NONE', 3,
 ( #5416, #17511, #16091, #12449, #1748, #7296, #5170, #12210 ),
 .UNSPECIFIED., .F., .F.,
 ( 4, 2, 2, 4 ),
 ( 0.002775112046897004661, 0.003466237704215408694, 0.004157363361533812293, 0.005539614676170621227 ),
 .UNSPECIFIED. ) ;
#7752=ADVANCED_FACE ( 'NONE', ( #7148 ), #4457, .T. ) ;
#7763=ORIENTED_EDGE ( 'NONE', *, *, #1878, .T. ) ;
#7785=EDGE_CURVE ( 'NONE', #3913, #6272, #341, .T. ) ;
#7791=ORIENTED_EDGE ( 'NONE', *, *, #9657, .T. ) ;
#7867=CIRCLE ( 'NONE', #10501, 4.750000000000000000 ) ;
#7940=VERTEX_POINT ( 'NONE', #11235 ) ;
#8034=CARTESIAN_POINT ( 'NONE',  ( -4.229990831856816236, -1.750000000000008882, 2.173440963673441750 ) ) ;
#8046=EDGE_CURVE ( 'NONE', #6638, #17782, #8250, .T. ) ;
#8050=CARTESIAN_POINT ( 'NONE',  ( 1.110223024625156540E-13, 1.749999999999998002, -4.750000000000000888 ) ) ;
#8065=ORIENTED_EDGE ( 'NONE', *, *, #13250, .F. ) ;
#8078=AXIS2_PLACEMENT_3D ( 'NONE', #8569, #21163, #5398 ) ;
#8105=CONICAL_SURFACE ( 'NONE', #976, 4.750000000000000888, 1.047197551196600074 ) ;
#8127=CARTESIAN_POINT ( 'NONE',  ( -0.9238745061264594938, 1.710161125106380631, 4.749999999999998224 ) ) ;
#8225=CARTESIAN_POINT ( 'NONE',  ( 2.742413778650823364, 1.749999999999998002, -4.750000000000024869 ) ) ;
#8242=DIRECTION ( 'NONE',  ( 0.000000000000000000, 1.000000000000000000, 0.000000000000000000 ) ) ;
#8250=CIRCLE ( 'NONE', #22525, 4.750000000000000888 ) ;
#8393=EDGE_CURVE ( 'NONE', #3763, #4916, #11376, .T. ) ;
#8492=EDGE_LOOP ( 'NONE', ( #11983, #20151, #12055 ) ) ;
#8493=VECTOR ( 'NONE', #9996, 1000.000000000000000 ) ;
#8494=ORIENTED_EDGE ( 'NONE', *, *, #18015, .T. ) ;
#8520=EDGE_CURVE ( 'NONE', #7692, #22215, #17291, .T. ) ;
#8569=CARTESIAN_POINT ( 'NONE',  ( 0.000000000000000000, -1.750000000000001554, 0.000000000000000000 ) ) ;
#8588=ORIENTED_EDGE ( 'NONE', *, *, #17555, .F. ) ;
#8590=CARTESIAN_POINT ( 'NONE',  ( 3.997250504095358981, -1.750000000000003331, 2.576559036326539154 ) ) ;
#8594=DIRECTION ( 'NONE',  ( 0.8660254037844385966, 0.000000000000000000, -0.5000000000000001110 ) ) ;
#8623=CARTESIAN_POINT ( 'NONE',  ( 4.229990831856820677, -1.750000000000000222, -2.173440963673463067 ) ) ;
#8661=DIRECTION ( 'NONE',  ( 0.000000000000000000, 1.000000000000000000, 0.000000000000000000 ) ) ;
#8674=CARTESIAN_POINT ( 'NONE',  ( 0.000000000000000000, -1.750000000000025757, 4.749999999999973355 ) ) ;
#8694=ADVANCED_FACE ( 'NONE', ( #12012 ), #17779, .T. ) ;
#8773=CIRCLE ( 'NONE', #1633, 4.750000000000000888 ) ;
#8783=DIRECTION ( 'NONE',  ( -8.438582421954109416E-32, 0.000000000000000000, -1.000000000000000000 ) ) ;
#8787=VERTEX_POINT ( 'NONE', #3558 ) ;
#8807=DIRECTION ( 'NONE',  ( 8.438582421954110511E-32, 0.000000000000000000, 1.000000000000000000 ) ) ;
#8865=CARTESIAN_POINT ( 'NONE',  ( 1.110223024625156540E-13, -1.750000000000001554, -4.750000000000000888 ) ) ;
#8888=SURFACE_STYLE_USAGE ( .BOTH. , #5601 ) ;
#8894=ORIENTED_EDGE ( 'NONE', *, *, #13262, .F. ) ;
#8903=ORIENTED_EDGE ( 'NONE', *, *, #456, .F. ) ;
#8910=CARTESIAN_POINT ( 'NONE',  ( 1.849731447993477218, -1.560358803165485586, 4.749999999999999112 ) ) ;
#8920=FACE_BOUND ( 'NONE', #5697, .T. ) ;
#8946=DIRECTION ( 'NONE',  ( 8.438582421954110511E-32, 0.000000000000000000, 1.000000000000000000 ) ) ;
#8977=CARTESIAN_POINT ( 'NONE',  ( 3.997250504095354984, 1.749999999999999556, -2.576559036326556917 ) ) ;
#8980=CARTESIAN_POINT ( 'NONE',  ( 4.692963726980105221, -1.672424706883760326, -1.371548386792676766 ) ) ;
#9045=CARTESIAN_POINT ( 'NONE',  ( -3.646393709166010577, 1.750000000000053291, -3.184260831324756680 ) ) ;
#9047=CARTESIAN_POINT ( 'NONE',  ( 0.000000000000000000, 1.750000000000001554, 0.000000000000000000 ) ) ;
#9076=CARTESIAN_POINT ( 'NONE',  ( -2.109645605488527628E-31, -1.750000000000001554, -2.500000000000000000 ) ) ;
#9157=EDGE_CURVE ( 'NONE', #8787, #18266, #7723, .T. ) ;
#9197=CARTESIAN_POINT ( 'NONE',  ( 0.000000000000000000, -1.750000000000001554, 0.000000000000000000 ) ) ;
#9253=EDGE_CURVE ( 'NONE', #13233, #3913, #15829, .T. ) ;
#9269=EDGE_CURVE ( 'NONE', #19664, #5108, #1639, .T. ) ;
#9290=DIRECTION ( 'NONE',  ( -8.438582421954109416E-32, 0.000000000000000000, -1.000000000000000000 ) ) ;
#9338=CARTESIAN_POINT ( 'NONE',  ( -4.578118944855300576, -1.701165921963301964, 1.570465384416986021 ) ) ;
#9339=ORIENTED_EDGE ( 'NONE', *, *, #21155, .F. ) ;
#9472=ORIENTED_EDGE ( 'NONE', *, *, #9253, .F. ) ;
#9492=CARTESIAN_POINT ( 'NONE',  ( -4.113620667976089607, 1.749999999999998002, -2.375000000000029754 ) ) ;
#9509=PLANE ( 'NONE',  #21280 ) ;
#9584=CARTESIAN_POINT ( 'NONE',  ( 0.4637351969133408636, 1.749999999999980904, -4.750000000000024869 ) ) ;
#9597=AXIS2_PLACEMENT_3D ( 'NONE', #2830, #15283, #15047 ) ;
#9622=ORIENTED_EDGE ( 'NONE', *, *, #21029, .F. ) ;
#9642=EDGE_CURVE ( 'NONE', #172, #7692, #2385, .T. ) ;
#9647=EDGE_LOOP ( 'NONE', ( #20545, #6952, #17760 ) ) ;
#9650=CARTESIAN_POINT ( 'NONE',  ( 1.849731447979666488, -1.560358803171614461, -4.750000000000024869 ) ) ;
#9657=EDGE_CURVE ( 'NONE', #226, #18733, #14186, .T. ) ;
#9682=CARTESIAN_POINT ( 'NONE',  ( -4.692963726980094563, -1.672424706883767875, 1.371548386792662333 ) ) ;
#9718=VERTEX_POINT ( 'NONE', #16638 ) ;
#9826=EDGE_LOOP ( 'NONE', ( #5168, #10056, #12330 ) ) ;
#9862=DIRECTION ( 'NONE',  ( -0.8660254037844384856, 0.000000000000000000, 0.5000000000000003331 ) ) ;
#9951=ORIENTED_EDGE ( 'NONE', *, *, #8046, .F. ) ;
#9957=CARTESIAN_POINT ( 'NONE',  ( 1.110223024625156540E-13, 1.749999999999998002, -4.750000000000000888 ) ) ;
#9996=DIRECTION ( 'NONE',  ( 0.000000000000000000, -1.000000000000000000, 0.000000000000000000 ) ) ;
#9997=FACE_OUTER_BOUND ( 'NONE', #20010, .T. ) ;
#10009=CARTESIAN_POINT ( 'NONE',  ( 0.000000000000000000, 1.750000000000001554, 0.000000000000000000 ) ) ;
#10056=ORIENTED_EDGE ( 'NONE', *, *, #10118, .F. ) ;
#10086=EDGE_LOOP ( 'NONE', ( #4890, #13825, #7008 ) ) ;
#10118=EDGE_CURVE ( 'NONE', #6272, #226, #20025, .T. ) ;
#10168=ORIENTED_EDGE ( 'NONE', *, *, #4941, .T. ) ;
#10226=CARTESIAN_POINT ( 'NONE',  ( 4.113620667976075396, -1.749999999999998002, -2.375000000000002220 ) ) ;
#10241=AXIS2_PLACEMENT_3D ( 'NONE', #1139, #15227, #6312 ) ;
#10255=DIRECTION ( 'NONE',  ( 0.000000000000000000, 1.000000000000000000, 0.000000000000000000 ) ) ;
#10329=AXIS2_PLACEMENT_3D ( 'NONE', #14490, #11291, #4115 ) ;
#10353=CARTESIAN_POINT ( 'NONE',  ( 0.000000000000000000, 1.750000000000001554, 0.000000000000000000 ) ) ;
#10430=AXIS2_PLACEMENT_3D ( 'NONE', #10009, #13885, #15757 ) ;
#10439=CARTESIAN_POINT ( 'NONE',  ( 0.4637351970278864033, -1.750000000000002665, 4.749999999999999112 ) ) ;
#10448=CARTESIAN_POINT ( 'NONE',  ( -4.113620667976089607, -1.750000000000001554, -2.375000000000005773 ) ) ;
#10451=DIRECTION ( 'NONE',  ( -0.000000000000000000, 1.000000000000000000, 0.000000000000000000 ) ) ;
#10466=CARTESIAN_POINT ( 'NONE',  ( -4.113620667976089607, 1.749999999999998002, -2.375000000000029754 ) ) ;
#10501=AXIS2_PLACEMENT_3D ( 'NONE', #19400, #8242, #22712 ) ;
#10511=( NAMED_UNIT ( * ) SI_UNIT ( $, .STERADIAN. ) SOLID_ANGLE_UNIT ( ) );
#10513=ORIENTED_EDGE ( 'NONE', *, *, #5437, .F. ) ;
#10529=LINE ( 'NONE', #13515, #17015 ) ;
#10633=AXIS2_PLACEMENT_3D ( 'NONE', #3090, #10255, #19317 ) ;
#10638=DIRECTION ( 'NONE',  ( -8.438582421954109416E-32, 0.000000000000000000, -1.000000000000000000 ) ) ;
#10680=DIRECTION ( 'NONE',  ( 0.000000000000000000, -1.000000000000000000, 0.000000000000000000 ) ) ;
#10742=FILL_AREA_STYLE_COLOUR ( '', #11987 ) ;
#10783=CARTESIAN_POINT ( 'NONE',  ( 0.000000000000000000, -1.750000000000001554, 0.000000000000000000 ) ) ;
#10807=DIRECTION ( 'NONE',  ( 8.438582421954109416E-32, 0.000000000000000000, 1.000000000000000000 ) ) ;
#10821=CARTESIAN_POINT ( 'NONE',  ( -3.880358743661353138, 1.739972214219164925, 2.779021504384385999 ) ) ;
#10833=ORIENTED_EDGE ( 'NONE', *, *, #11811, .F. ) ;
#10848=CARTESIAN_POINT ( 'NONE',  ( 5.484827557301438894, 1.749999999999998002, -2.775557561562891351E-14 ) ) ;
#10864=ORIENTED_EDGE ( 'NONE', *, *, #1875, .T. ) ;
#10874=( LENGTH_UNIT ( ) NAMED_UNIT ( * ) SI_UNIT ( .MILLI., .METRE. ) );
#10902=EDGE_CURVE ( 'NONE', #7692, #8787, #13238, .T. ) ;
#10924=CARTESIAN_POINT ( 'NONE',  ( -3.191783008269886146, 1.561572887838377666, 3.971669662941508694 ) ) ;
#10963=UNCERTAINTY_MEASURE_WITH_UNIT (LENGTH_MEASURE( 1.000000000000000082E-05 ), #10874, 'distance_accuracy_value', 'NONE');
#10986=FILL_AREA_STYLE ('',( #7358 ) ) ;
#10998=AXIS2_PLACEMENT_3D ( 'NONE', #21368, #17462, #22768 ) ;
#11004=ORIENTED_EDGE ( 'NONE', *, *, #18844, .T. ) ;
#11090=CARTESIAN_POINT ( 'NONE',  ( -4.346882592290802982, -1.739972214219165370, 1.970978495615605341 ) ) ;
#11107=CONICAL_SURFACE ( 'NONE', #14491, 4.750000000000000888, 1.047197551196600074 ) ;
#11137=B_SPLINE_CURVE_WITH_KNOTS ( 'NONE', 3,
 ( #17318, #1796, #14039, #19800, #19331, #21231, #1450, #19440 ),
 .UNSPECIFIED., .F., .F.,
 ( 4, 2, 2, 4 ),
 ( 0.002775112046897006829, 0.003466237704215410428, 0.004157363361533814895, 0.005539614676170622962 ),
 .UNSPECIFIED. ) ;
#11164=ADVANCED_FACE ( 'NONE', ( #20788 ), #1251, .F. ) ;
#11230=CIRCLE ( 'NONE', #2211, 4.750000000000000000 ) ;
#11235=CARTESIAN_POINT ( 'NONE',  ( 5.484827557301452217, -1.325747111984059590, 0.000000000000000000 ) ) ;
#11269=DIRECTION ( 'NONE',  ( 0.000000000000000000, 1.000000000000000000, 0.000000000000000000 ) ) ;
#11291=DIRECTION ( 'NONE',  ( 0.000000000000000000, -1.000000000000000000, 0.000000000000000000 ) ) ;
#11376=B_SPLINE_CURVE_WITH_KNOTS ( 'NONE', 3,
 ( #281, #19139, #19251, #14082 ),
 .UNSPECIFIED., .F., .F.,
 ( 4, 4 ),
 ( 2.380735702043565917E-07, 0.002775112046897006395 ),
 .UNSPECIFIED. ) ;
#11380=FACE_OUTER_BOUND ( 'NONE', #829, .T. ) ;
#11405=ORIENTED_EDGE ( 'NONE', *, *, #4332, .F. ) ;
#11407=CARTESIAN_POINT ( 'NONE',  ( 0.4637351969133413077, -1.749999999999980904, -4.750000000000023981 ) ) ;
#11603=ORIENTED_EDGE ( 'NONE', *, *, #22762, .T. ) ;
#11694=ORIENTED_EDGE ( 'NONE', *, *, #21348, .T. ) ;
#11761=DIRECTION ( 'NONE',  ( 0.000000000000000000, 1.000000000000000000, 0.000000000000000000 ) ) ;
#11811=EDGE_CURVE ( 'NONE', #4916, #16467, #3148, .T. ) ;
#11890=CARTESIAN_POINT ( 'NONE',  ( 0.000000000000000000, -1.750000000000025757, 4.749999999999973355 ) ) ;
#11900=CARTESIAN_POINT ( 'NONE',  ( -2.742413778650712342, -1.325747111984083793, 4.749999999999999112 ) ) ;
#11983=ORIENTED_EDGE ( 'NONE', *, *, #1779, .T. ) ;
#11987=COLOUR_RGB ( '', 0.66274510, 0.83137255, 0.94901961) ;
#12012=FACE_OUTER_BOUND ( 'NONE', #9647, .T. ) ;
#12055=ORIENTED_EDGE ( 'NONE', *, *, #22762, .F. ) ;
#12210=CARTESIAN_POINT ( 'NONE',  ( -2.742413778650615086, -1.325747111984059590, -4.749999999999997335 ) ) ;
#12221=FACE_OUTER_BOUND ( 'NONE', #1209, .T. ) ;
#12260=( LENGTH_UNIT ( ) NAMED_UNIT ( * ) SI_UNIT ( .MILLI., .METRE. ) );
#12330=ORIENTED_EDGE ( 'NONE', *, *, #21029, .T. ) ;
#12360=ORIENTED_EDGE ( 'NONE', *, *, #20352, .T. ) ;
#12403=DIRECTION ( 'NONE',  ( 0.000000000000000000, -1.000000000000000000, 0.000000000000000000 ) ) ;
#12445=ORIENTED_EDGE ( 'NONE', *, *, #7785, .T. ) ;
#12449=CARTESIAN_POINT ( 'NONE',  ( -3.649122391096772500, -1.701165921963347705, -3.179534615582980894 ) ) ;
#12469=AXIS2_PLACEMENT_3D ( 'NONE', #18448, #9862, #7633 ) ;
#12518=CARTESIAN_POINT ( 'NONE',  ( -2.742413778650615086, 1.750000000000001554, -4.750000000000004441 ) ) ;
#12558=CARTESIAN_POINT ( 'NONE',  ( 0.000000000000000000, 1.750000000000001554, 0.000000000000000000 ) ) ;
#12581=CARTESIAN_POINT ( 'NONE',  ( -0.9238745060512592033, -1.710161125114598946, -4.750000000000025757 ) ) ;
#12620=EDGE_LOOP ( 'NONE', ( #11694, #17338, #18496 ) ) ;
#12638=( NAMED_UNIT ( * ) PLANE_ANGLE_UNIT ( ) SI_UNIT ( $, .RADIAN. ) );
#12662=DIRECTION ( 'NONE',  ( 8.438582421954109416E-32, 0.000000000000000000, 1.000000000000000000 ) ) ;
#12699=CARTESIAN_POINT ( 'NONE',  ( -5.484827557301452217, 1.749999999999973799, -2.775557561562891351E-14 ) ) ;
#12701=CARTESIAN_POINT ( 'NONE',  ( -5.484827557301452217, 1.749999999999973799, -2.775557561562891351E-14 ) ) ;
#12730=CARTESIAN_POINT ( 'NONE',  ( 2.742413778650823364, 1.325747111984056037, -4.750000000000000888 ) ) ;
#12864=ORIENTED_EDGE ( 'NONE', *, *, #15747, .F. ) ;
#12897=B_SPLINE_CURVE_WITH_KNOTS ( 'NONE', 3,
 ( #7184, #7409, #5423, #12581, #19766, #14578 ),
 .UNSPECIFIED., .F., .F.,
 ( 4, 2, 4 ),
 ( 0.004904497004059944938, 0.006291728891672870860, 0.007678960779285795915 ),
 .UNSPECIFIED. ) ;
#12985=CARTESIAN_POINT ( 'NONE',  ( -5.484827557301438894, -1.325747111984083793, 0.000000000000000000 ) ) ;
#12995=CARTESIAN_POINT ( 'NONE',  ( 2.298974087852387438, 1.453757124409940760, -4.750000000000023981 ) ) ;
#13039=DIRECTION ( 'NONE',  ( 8.438582421954110511E-32, 0.000000000000000000, 1.000000000000000000 ) ) ;
#13120=AXIS2_PLACEMENT_3D ( 'NONE', #21609, #14427, #86 ) ;
#13187=ORIENTED_EDGE ( 'NONE', *, *, #22835, .F. ) ;
#13209=CARTESIAN_POINT ( 'NONE',  ( -5.261076337303407513, -1.454929939081825108, 0.3875484812921078936 ) ) ;
#13233=VERTEX_POINT ( 'NONE', #1186 ) ;
#13238=CIRCLE ( 'NONE', #107, 4.750000000000000888 ) ;
#13250=EDGE_CURVE ( 'NONE', #16377, #3913, #7867, .T. ) ;
#13262=EDGE_CURVE ( 'NONE', #13441, #17782, #14874, .T. ) ;
#13267=ORIENTED_EDGE ( 'NONE', *, *, #14589, .T. ) ;
#13399=COLOUR_RGB ( '', 0.66274510, 0.83137255, 0.94901961) ;
#13441=VERTEX_POINT ( 'NONE', #22101 ) ;
#13515=CARTESIAN_POINT ( 'NONE',  ( 2.742413778650726108, 1.750000000000001554, 4.750000000000000888 ) ) ;
#13576=DIRECTION ( 'NONE',  ( 8.438582421954109416E-32, 0.000000000000000000, 1.000000000000000000 ) ) ;
#13589=ORIENTED_EDGE ( 'NONE', *, *, #10118, .T. ) ;
#13614=ORIENTED_EDGE ( 'NONE', *, *, #11811, .T. ) ;
#13726=DIRECTION ( 'NONE',  ( 8.438582421954109416E-32, 0.000000000000000000, 1.000000000000000000 ) ) ;
#13771=CARTESIAN_POINT ( 'NONE',  ( 3.880358743661374010, -1.739972214219160263, 2.779021504384370900 ) ) ;
#13825=ORIENTED_EDGE ( 'NONE', *, *, #18898, .F. ) ;
#13835=CARTESIAN_POINT ( 'NONE',  ( 2.742413778650726108, 1.325747111984056037, 4.749999999999997335 ) ) ;
#13880=MECHANICAL_DESIGN_GEOMETRIC_PRESENTATION_REPRESENTATION('',(#22518),#1472);
#13882=CARTESIAN_POINT ( 'NONE',  ( 3.191035955565536320, -1.584759246591021187, -3.972963596181403378 ) ) ;
#13885=DIRECTION ( 'NONE',  ( 0.000000000000000000, 1.000000000000000000, 0.000000000000000000 ) ) ;
#13907=DIRECTION ( 'NONE',  ( 0.000000000000000000, -1.000000000000000000, 0.000000000000000000 ) ) ;
#13921=( LENGTH_UNIT ( ) NAMED_UNIT ( * ) SI_UNIT ( .MILLI., .METRE. ) );
#13923=EDGE_LOOP ( 'NONE', ( #11603, #11004, #14708, #21921, #5193, #1695 ) ) ;
#13940=CARTESIAN_POINT ( 'NONE',  ( -1.839530896184778719, -1.562503694739640014, 4.749999999999998224 ) ) ;
#13999=PRODUCT ( 'Nut', 'Nut', '', ( #245 ) ) ;
#14039=CARTESIAN_POINT ( 'NONE',  ( 4.346882592290811864, 1.739972214219157598, 1.970978495615613113 ) ) ;
#14082=CARTESIAN_POINT ( 'NONE',  ( 4.113620667976075396, 1.750000000000001554, -2.375000000000002220 ) ) ;
#14108=AXIS2_PLACEMENT_3D ( 'NONE', #9047, #14465, #10807 ) ;
#14175=VERTEX_POINT ( 'NONE', #9076 ) ;
#14186=B_SPLINE_CURVE_WITH_KNOTS ( 'NONE', 3,
 ( #7156, #1387, #5387, #1837, #15609, #6680 ),
 .UNSPECIFIED., .F., .F.,
 ( 4, 2, 4 ),
 ( 0.007678960753836396383, 0.009067029700227515615, 0.01045509864661863311 ),
 .UNSPECIFIED. ) ;
#14245=CARTESIAN_POINT ( 'NONE',  ( -3.649122391096853324, 1.701165921963302408, 3.179534615583007984 ) ) ;
#14254=ORIENTED_EDGE ( 'NONE', *, *, #20352, .F. ) ;
#14347=FACE_OUTER_BOUND ( 'NONE', #17090, .T. ) ;
#14351=CARTESIAN_POINT ( 'NONE',  ( -2.742413778650712342, 1.325747111984031834, 4.749999999999999112 ) ) ;
#14370=DIRECTION ( 'NONE',  ( 0.000000000000000000, 1.000000000000000000, 0.000000000000000000 ) ) ;
#14389=SURFACE_SIDE_STYLE ('',( #6873 ) ) ;
#14427=DIRECTION ( 'NONE',  ( 0.000000000000000000, 1.000000000000000000, 0.000000000000000000 ) ) ;
#14438=CARTESIAN_POINT ( 'NONE',  ( -4.113620667976075396, 1.749999999999998002, 2.374999999999998668 ) ) ;
#14446=CARTESIAN_POINT ( 'NONE',  ( 0.000000000000000000, -1.750000000000001554, 0.000000000000000000 ) ) ;
#14465=DIRECTION ( 'NONE',  ( 0.000000000000000000, -1.000000000000000000, 0.000000000000000000 ) ) ;
#14467=CIRCLE ( 'NONE', #6950, 2.500000000000000000 ) ;
#14490=CARTESIAN_POINT ( 'NONE',  ( 0.000000000000000000, 1.750000000000001554, 0.000000000000000000 ) ) ;
#14491=AXIS2_PLACEMENT_3D ( 'NONE', #14446, #18316, #5624 ) ;
#14578=CARTESIAN_POINT ( 'NONE',  ( 1.110223024625156540E-13, -1.750000000000001554, -4.750000000000000888 ) ) ;
#14589=EDGE_CURVE ( 'NONE', #1642, #22215, #14687, .T. ) ;
#14610=CARTESIAN_POINT ( 'NONE',  ( 3.534277608972077545, 1.672424706883760770, -3.378451613207327231 ) ) ;
#14641=CARTESIAN_POINT ( 'NONE',  ( 0.9337610948747044892, 1.709055945004937405, -4.750000000000024869 ) ) ;
#14643=B_SPLINE_CURVE_WITH_KNOTS ( 'NONE', 3,
 ( #20850, #2953, #17052, #8127, #1312, #6370 ),
 .UNSPECIFIED., .F., .F.,
 ( 4, 2, 4 ),
 ( 0.004904496978749070882, 0.006291728866292733632, 0.007678960753836396383 ),
 .UNSPECIFIED. ) ;
#14648=ORIENTED_EDGE ( 'NONE', *, *, #2784, .T. ) ;
#14687=LINE ( 'NONE', #12699, #6791 ) ;
#14708=ORIENTED_EDGE ( 'NONE', *, *, #10902, .T. ) ;
#14790=CARTESIAN_POINT ( 'NONE',  ( -4.229990831856726530, 1.750000000000057732, -2.173440963673431536 ) ) ;
#14859=CARTESIAN_POINT ( 'NONE',  ( -4.113620667976075396, -1.750000000000001554, 2.374999999999986677 ) ) ;
#14874=B_SPLINE_CURVE_WITH_KNOTS ( 'NONE', 3,
 ( #19059, #13882, #4709, #10226 ),
 .UNSPECIFIED., .F., .F.,
 ( 4, 4 ),
 ( 2.380735702043793293E-07, 0.002775112046896986880 ),
 .UNSPECIFIED. ) ;
#14936=ORIENTED_EDGE ( 'NONE', *, *, #456, .T. ) ;
#14995=ADVANCED_FACE ( 'NONE', ( #323 ), #2670, .T. ) ;
#15047=DIRECTION ( 'NONE',  ( -8.438582421954110511E-32, 0.000000000000000000, -1.000000000000000000 ) ) ;
#15079=APPLICATION_CONTEXT ( 'automotive_design' ) ;
#15088=DIRECTION ( 'NONE',  ( 0.000000000000000000, 1.000000000000000000, 0.000000000000000000 ) ) ;
#15141=AXIS2_PLACEMENT_3D ( 'NONE', #23049, #10451, #8807 ) ;
#15214=UNCERTAINTY_MEASURE_WITH_UNIT (LENGTH_MEASURE( 1.000000000000000082E-05 ), #12260, 'distance_accuracy_value', 'NONE');
#15227=DIRECTION ( 'NONE',  ( 0.000000000000000000, -1.000000000000000000, 0.000000000000000000 ) ) ;
#15264=STYLED_ITEM ( 'NONE', ( #16506 ), #5146 ) ;
#15265=EDGE_CURVE ( 'NONE', #7940, #21726, #16085, .T. ) ;
#15281=ORIENTED_EDGE ( 'NONE', *, *, #8520, .F. ) ;
#15283=DIRECTION ( 'NONE',  ( 0.000000000000000000, -1.000000000000000000, 0.000000000000000000 ) ) ;
#15287=CARTESIAN_POINT ( 'NONE',  ( 3.649122391096873752, -1.701165921963298633, 3.179534615582995105 ) ) ;
#15318=ORIENTED_EDGE ( 'NONE', *, *, #15265, .F. ) ;
#15452=ORIENTED_EDGE ( 'NONE', *, *, #8393, .F. ) ;
#15521=CARTESIAN_POINT ( 'NONE',  ( 4.113620667976089607, -1.750000000000025757, 2.374999999999986677 ) ) ;
#15528=DIRECTION ( 'NONE',  ( 0.000000000000000000, 1.000000000000000000, 0.000000000000000000 ) ) ;
#15557=CARTESIAN_POINT ( 'NONE',  ( -2.742413778650712342, 1.749999999999973799, 4.749999999999999112 ) ) ;
#15594=CARTESIAN_POINT ( 'NONE',  ( 0.000000000000000000, 1.750000000000001554, 0.000000000000000000 ) ) ;
#15609=CARTESIAN_POINT ( 'NONE',  ( 2.298974087845766956, 1.453757124411862778, 4.749999999999999112 ) ) ;
#15642=DIRECTION ( 'NONE',  ( 8.438582421954109416E-32, 0.000000000000000000, 1.000000000000000000 ) ) ;
#15683=CIRCLE ( 'NONE', #10430, 4.750000000000000000 ) ;
#15697=CARTESIAN_POINT ( 'NONE',  ( 5.036205380386659769, -1.584759246591014747, 0.7770364038185700872 ) ) ;
#15747=EDGE_CURVE ( 'NONE', #19664, #14175, #1439, .T. ) ;
#15757=DIRECTION ( 'NONE',  ( 8.438582421954109416E-32, 0.000000000000000000, 1.000000000000000000 ) ) ;
#15760=DIRECTION ( 'NONE',  ( -0.5000000000000001110, 0.000000000000000000, -0.8660254037844385966 ) ) ;
#15814=CARTESIAN_POINT ( 'NONE',  ( 3.191035955565519888, 1.584759246591017634, 3.972963596181424695 ) ) ;
#15829=B_SPLINE_CURVE_WITH_KNOTS ( 'NONE', 3,
 ( #3639, #1861, #9045, #10466 ),
 .UNSPECIFIED., .F., .F.,
 ( 4, 4 ),
 ( 2.380735702043732148E-07, 0.002775112046897002492 ),
 .UNSPECIFIED. ) ;
#15935=CARTESIAN_POINT ( 'NONE',  ( 4.113620667976089607, 1.749999999999973799, 2.375000000000000444 ) ) ;
#15947=ORIENTED_EDGE ( 'NONE', *, *, #17555, .T. ) ;
#15953=ADVANCED_FACE ( 'NONE', ( #4317 ), #18568, .F. ) ;
#15962=DIRECTION ( 'NONE',  ( -8.438582421954109416E-32, 0.000000000000000000, -1.000000000000000000 ) ) ;
#16077=CARTESIAN_POINT ( 'NONE',  ( 0.000000000000000000, -1.750000000000001554, 0.000000000000000000 ) ) ;
#16078=CARTESIAN_POINT ( 'NONE',  ( -4.113620667976075396, 1.749999999999998002, 2.374999999999998668 ) ) ;
#16085=B_SPLINE_CURVE_WITH_KNOTS ( 'NONE', 3,
 ( #18896, #15697, #17469, #21255 ),
 .UNSPECIFIED., .F., .F.,
 ( 4, 4 ),
 ( 2.380735702001470497E-07, 0.002775112046897012467 ),
 .UNSPECIFIED. ) ;
#16091=CARTESIAN_POINT ( 'NONE',  ( -3.880358743661276755, -1.739972214219213109, -2.779021504384352248 ) ) ;
#16141=PRESENTATION_STYLE_ASSIGNMENT (( #3235 ) ) ;
#16203=FACE_OUTER_BOUND ( 'NONE', #2380, .T. ) ;
#16213=PLANE ( 'NONE',  #3204 ) ;
#16220=SHAPE_DEFINITION_REPRESENTATION ( #20953, #17033 ) ;
#16237=CARTESIAN_POINT ( 'NONE',  ( 0.000000000000000000, -1.750000000000001554, 0.000000000000000000 ) ) ;
#16242=LINE ( 'NONE', #10848, #4655 ) ;
#16255=B_SPLINE_CURVE_WITH_KNOTS ( 'NONE', 3,
 ( #17852, #5025, #17724, #14438 ),
 .UNSPECIFIED., .F., .F.,
 ( 4, 4 ),
 ( 2.380735702043570947E-07, 0.002775112046897009431 ),
 .UNSPECIFIED. ) ;
#16301=CIRCLE ( 'NONE', #19311, 2.500000000000000000 ) ;
#16330=AXIS2_PLACEMENT_3D ( 'NONE', #707, #4101, #9290 ) ;
#16377=VERTEX_POINT ( 'NONE', #9957 ) ;
#16413=DIRECTION ( 'NONE',  ( 0.000000000000000000, -1.000000000000000000, 0.000000000000000000 ) ) ;
#16466=ORIENTED_EDGE ( 'NONE', *, *, #9269, .F. ) ;
#16467=VERTEX_POINT ( 'NONE', #18892 ) ;
#16477=CARTESIAN_POINT ( 'NONE',  ( 3.880358743661364240, 1.739972214219156044, -2.779021504384395325 ) ) ;
#16479=CARTESIAN_POINT ( 'NONE',  ( -2.742413778650615086, -1.325747111984059590, -4.749999999999997335 ) ) ;
#16506=PRESENTATION_STYLE_ASSIGNMENT (( #8888 ) ) ;
#16541=EDGE_CURVE ( 'NONE', #17782, #21726, #6121, .T. ) ;
#16635=ORIENTED_EDGE ( 'NONE', *, *, #2050, .F. ) ;
#16638=CARTESIAN_POINT ( 'NONE',  ( -2.742413778650712342, 1.325747111984031834, 4.749999999999999112 ) ) ;
#16654=CARTESIAN_POINT ( 'NONE',  ( -5.261076337303340900, 1.454929939081866186, -0.3875484812920578226 ) ) ;
#16673=VERTEX_POINT ( 'NONE', #410 ) ;
#16701=DIRECTION ( 'NONE',  ( 0.000000000000000000, 1.000000000000000000, 0.000000000000000000 ) ) ;
#16967=CARTESIAN_POINT ( 'NONE',  ( -0.4634555468559497515, 1.749999999999992673, -4.750000000000023093 ) ) ;
#17015=VECTOR ( 'NONE', #19471, 1000.000000000000000 ) ;
#17033=SHAPE_REPRESENTATION ( 'Nut', ( #22115 ), #18753 ) ;
#17052=CARTESIAN_POINT ( 'NONE',  ( -1.839530896184789155, 1.562503694739638016, 4.749999999999999112 ) ) ;
#17090=EDGE_LOOP ( 'NONE', ( #13589, #7763, #10864, #18999, #17357, #12445 ) ) ;
#17143=MECHANICAL_DESIGN_GEOMETRIC_PRESENTATION_REPRESENTATION('',(#15264),#18505);
#17209=CARTESIAN_POINT ( 'NONE',  ( 0.000000000000000000, -1.750000000000001554, 0.000000000000000000 ) ) ;
#17211=EDGE_CURVE ( 'NONE', #9718, #226, #14643, .T. ) ;
#17262=LINE ( 'NONE', #8225, #2063 ) ;
#17291=B_SPLINE_CURVE_WITH_KNOTS ( 'NONE', 3,
 ( #14859, #8034, #11090, #9338, #9682, #22267, #13209, #12985 ),
 .UNSPECIFIED., .F., .F.,
 ( 4, 2, 2, 4 ),
 ( 0.002775112046897000757, 0.003466237704215407826, 0.004157363361533814028, 0.005539614676170626431 ),
 .UNSPECIFIED. ) ;
#17312=DIRECTION ( 'NONE',  ( 0.000000000000000000, -1.000000000000000000, 0.000000000000000000 ) ) ;
#17318=CARTESIAN_POINT ( 'NONE',  ( 4.113620667976089607, 1.749999999999973799, 2.375000000000000444 ) ) ;
#17338=ORIENTED_EDGE ( 'NONE', *, *, #1199, .T. ) ;
#17357=ORIENTED_EDGE ( 'NONE', *, *, #13250, .T. ) ;
#17386=ORIENTED_EDGE ( 'NONE', *, *, #17211, .F. ) ;
#17396=EDGE_LOOP ( 'NONE', ( #17386, #18418, #20152, #21031, #8588, #21136 ) ) ;
#17460=CONICAL_SURFACE ( 'NONE', #10329, 4.750000000000000000, 1.047197551196600074 ) ;
#17462=DIRECTION ( 'NONE',  ( 0.000000000000000000, 1.000000000000000000, 0.000000000000000000 ) ) ;
#17469=CARTESIAN_POINT ( 'NONE',  ( 4.580847626786066940, -1.750000000000001110, 1.565739168675225779 ) ) ;
#17470=CARTESIAN_POINT ( 'NONE',  ( -2.742413778650712342, -1.325747111984083793, 4.749999999999999112 ) ) ;
#17487=AXIS2_PLACEMENT_3D ( 'NONE', #1084, #6800, #17618 ) ;
#17499=FACE_OUTER_BOUND ( 'NONE', #3203, .T. ) ;
#17511=CARTESIAN_POINT ( 'NONE',  ( -3.997250504095275048, -1.750000000000057288, -2.576559036326496965 ) ) ;
#17555=EDGE_CURVE ( 'NONE', #18733, #16673, #10529, .T. ) ;
#17587=CARTESIAN_POINT ( 'NONE',  ( -2.296348136192885026, -1.454515171358716552, 4.749999999999999112 ) ) ;
#17618=DIRECTION ( 'NONE',  ( -1.000000000000000000, 0.000000000000000000, -8.438582421954110511E-32 ) ) ;
#17653=ORIENTED_EDGE ( 'NONE', *, *, #13262, .T. ) ;
#17680=( NAMED_UNIT ( * ) PLANE_ANGLE_UNIT ( ) SI_UNIT ( $, .RADIAN. ) );
#17724=CARTESIAN_POINT ( 'NONE',  ( -4.580847626786052729, 1.750000000000008438, 1.565739168675228221 ) ) ;
#17760=ORIENTED_EDGE ( 'NONE', *, *, #16541, .F. ) ;
#17779=CONICAL_SURFACE ( 'NONE', #10633, 4.750000000000000888, 1.047197551196600074 ) ;
#17782=VERTEX_POINT ( 'NONE', #2401 ) ;
#17821=ORIENTED_EDGE ( 'NONE', *, *, #22835, .T. ) ;
#17852=CARTESIAN_POINT ( 'NONE',  ( -5.484827557301438894, 1.325747111984031834, 0.000000000000000000 ) ) ;
#17858=CARTESIAN_POINT ( 'NONE',  ( 4.113620667976075396, 1.750000000000001554, -2.375000000000002220 ) ) ;
#17892=CARTESIAN_POINT ( 'NONE',  ( -4.113620667976075396, 1.749999999999998002, 2.374999999999998668 ) ) ;
#17916=CARTESIAN_POINT ( 'NONE',  ( 4.113620667976075396, 1.750000000000001554, -2.375000000000002220 ) ) ;
#17926=SHAPE_REPRESENTATION_RELATIONSHIP ( 'NONE' , 'NONE' ,  #17033, #3025 ) ;
#18012=CARTESIAN_POINT ( 'NONE',  ( -2.966164998648741058, 1.454929939081821999, 4.362451518707897158 ) ) ;
#18015=EDGE_CURVE ( 'NONE', #3763, #7940, #16242, .T. ) ;
#18028=FACE_OUTER_BOUND ( 'NONE', #18419, .T. ) ;
#18034=CARTESIAN_POINT ( 'NONE',  ( 3.649122391096871532, 1.701165921963294858, -3.179534615583005763 ) ) ;
#18038=CARTESIAN_POINT ( 'NONE',  ( 4.578118944855307682, -1.701165921963294858, -1.570465384417001786 ) ) ;
#18067=( NAMED_UNIT ( * ) SI_UNIT ( $, .STERADIAN. ) SOLID_ANGLE_UNIT ( ) );
#18093=CARTESIAN_POINT ( 'NONE',  ( -4.692963726980019956, 1.672424706883815393, -1.371548386792625696 ) ) ;
#18095=DIRECTION ( 'NONE',  ( -0.5000000000000001110, -1.577721810442023611E-30, 0.8660254037844385966 ) ) ;
#18143=B_SPLINE_CURVE_WITH_KNOTS ( 'NONE', 3,
 ( #6655, #19234, #1372, #13940, #17587, #17470 ),
 .UNSPECIFIED., .F., .F.,
 ( 4, 2, 4 ),
 ( 0.004766700742568914795, 0.006150321122490677583, 0.007533941502412439505 ),
 .UNSPECIFIED. ) ;
#18256=CARTESIAN_POINT ( 'NONE',  ( 3.191783008269916344, 1.561572887838375445, -3.971669662941486045 ) ) ;
#18266=VERTEX_POINT ( 'NONE', #16479 ) ;
#18302=EDGE_LOOP ( 'NONE', ( #10168, #19700, #21465 ) ) ;
#18311=EDGE_CURVE ( 'NONE', #4916, #16377, #2795, .T. ) ;
#18316=DIRECTION ( 'NONE',  ( 0.000000000000000000, 1.000000000000000000, 0.000000000000000000 ) ) ;
#18327=CONICAL_SURFACE ( 'NONE', #7074, 4.750000000000000888, 1.047197551196600074 ) ;
#18331=AXIS2_PLACEMENT_3D ( 'NONE', #17209, #6522, #2516 ) ;
#18364=APPLICATION_CONTEXT ( 'automotive_design' ) ;
#18418=ORIENTED_EDGE ( 'NONE', *, *, #19543, .T. ) ;
#18419=EDGE_LOOP ( 'NONE', ( #7791, #22647, #22209 ) ) ;
#18448=CARTESIAN_POINT ( 'NONE',  ( 5.484827557301438894, 1.749999999999998002, -2.775557561562891351E-14 ) ) ;
#18490=CARTESIAN_POINT ( 'NONE',  ( -5.484827557301438894, -1.325747111984083793, 0.000000000000000000 ) ) ;
#18496=ORIENTED_EDGE ( 'NONE', *, *, #7785, .F. ) ;
#18505=( GEOMETRIC_REPRESENTATION_CONTEXT ( 3 ) GLOBAL_UNCERTAINTY_ASSIGNED_CONTEXT ( ( #10963 ) ) GLOBAL_UNIT_ASSIGNED_CONTEXT ( ( #10874, #12638, #18067 ) ) REPRESENTATION_CONTEXT ( 'NONE', 'WORKASPACE' ) );
#18551=CARTESIAN_POINT ( 'NONE',  ( -4.578118944855224193, 1.701165921963350813, -1.570465384416952936 ) ) ;
#18568=PLANE ( 'NONE',  #12469 ) ;
#18733=VERTEX_POINT ( 'NONE', #22461 ) ;
#18753=( GEOMETRIC_REPRESENTATION_CONTEXT ( 3 ) GLOBAL_UNCERTAINTY_ASSIGNED_CONTEXT ( ( #15214 ) ) GLOBAL_UNIT_ASSIGNED_CONTEXT ( ( #12260, #17680, #10511 ) ) REPRESENTATION_CONTEXT ( 'NONE', 'WORKASPACE' ) );
#18754=CARTESIAN_POINT ( 'NONE',  ( 0.000000000000000000, 1.750000000000001554, 0.000000000000000000 ) ) ;
#18770=ORIENTED_EDGE ( 'NONE', *, *, #18311, .F. ) ;
#18789=B_SPLINE_CURVE_WITH_KNOTS ( 'NONE', 3,
 ( #13835, #15814, #1594, #15935 ),
 .UNSPECIFIED., .F., .F.,
 ( 4, 4 ),
 ( 2.380735702073125514E-07, 0.002775112046897006829 ),
 .UNSPECIFIED. ) ;
#18810=DIRECTION ( 'NONE',  ( 0.000000000000000000, -1.000000000000000000, 0.000000000000000000 ) ) ;
#18844=EDGE_CURVE ( 'NONE', #23235, #7692, #20412, .T. ) ;
#18879=ADVANCED_FACE ( 'NONE', ( #8920, #19265 ), #3402, .F. ) ;
#18889=ADVANCED_FACE ( 'NONE', ( #17499 ), #7644, .T. ) ;
#18892=CARTESIAN_POINT ( 'NONE',  ( 2.742413778650823364, 1.325747111984056037, -4.750000000000000888 ) ) ;
#18896=CARTESIAN_POINT ( 'NONE',  ( 5.484827557301452217, -1.325747111984059590, 0.000000000000000000 ) ) ;
#18898=EDGE_CURVE ( 'NONE', #8787, #6638, #8773, .T. ) ;
#18917=AXIS2_PLACEMENT_3D ( 'NONE', #12558, #1735, #21408 ) ;
#18951=CARTESIAN_POINT ( 'NONE',  ( 3.191783008269905686, -1.561572887838375889, 3.971669662941499368 ) ) ;
#18999=ORIENTED_EDGE ( 'NONE', *, *, #18311, .T. ) ;
#19002=CONICAL_SURFACE ( 'NONE', #14108, 4.750000000000000000, 1.047197551196600074 ) ;
#19058=FACE_OUTER_BOUND ( 'NONE', #7201, .T. ) ;
#19059=CARTESIAN_POINT ( 'NONE',  ( 2.742413778650823364, -1.325747111984059590, -4.750000000000000888 ) ) ;
#19099=DIRECTION ( 'NONE',  ( 0.000000000000000000, -1.000000000000000000, 0.000000000000000000 ) ) ;
#19139=CARTESIAN_POINT ( 'NONE',  ( 5.036205380386656216, 1.584759246591015414, -0.7770364038185831879 ) ) ;
#19161=CARTESIAN_POINT ( 'NONE',  ( 2.742413778650823364, 1.749999999999998002, -4.750000000000024869 ) ) ;
#19234=CARTESIAN_POINT ( 'NONE',  ( -0.4634555469063539879, -1.750000000000002220, 4.749999999999999112 ) ) ;
#19251=CARTESIAN_POINT ( 'NONE',  ( 4.580847626786062499, 1.750000000000000222, -1.565739168675242210 ) ) ;
#19255=CARTESIAN_POINT ( 'NONE',  ( 2.742413778650726108, -1.325747111984059590, 4.749999999999997335 ) ) ;
#19265=FACE_OUTER_BOUND ( 'NONE', #13923, .T. ) ;
#19268=CARTESIAN_POINT ( 'NONE',  ( 3.061616997868385113E-16, 1.750000000000001554, 2.500000000000000000 ) ) ;
#19311=AXIS2_PLACEMENT_3D ( 'NONE', #4122, #16701, #20364 ) ;
#19317=DIRECTION ( 'NONE',  ( -8.438582421954109416E-32, 0.000000000000000000, -1.000000000000000000 ) ) ;
#19324=EDGE_CURVE ( 'NONE', #18733, #5138, #18789, .T. ) ;
#19331=CARTESIAN_POINT ( 'NONE',  ( 4.692963726980105221, 1.672424706883761658, 1.371548386792669438 ) ) ;
#19388=CARTESIAN_POINT ( 'NONE',  ( 2.742413778650726108, 1.750000000000001554, 4.750000000000000888 ) ) ;
#19400=CARTESIAN_POINT ( 'NONE',  ( 0.000000000000000000, 1.750000000000001554, 0.000000000000000000 ) ) ;
#19434=DIRECTION ( 'NONE',  ( -8.438582421954109416E-32, 0.000000000000000000, -1.000000000000000000 ) ) ;
#19440=CARTESIAN_POINT ( 'NONE',  ( 5.484827557301438894, 1.325747111984056037, 0.000000000000000000 ) ) ;
#19469=CARTESIAN_POINT ( 'NONE',  ( 0.000000000000000000, -1.750000000000001554, 0.000000000000000000 ) ) ;
#19471=DIRECTION ( 'NONE',  ( 0.000000000000000000, -1.000000000000000000, 0.000000000000000000 ) ) ;
#19543=EDGE_CURVE ( 'NONE', #9718, #172, #6621, .T. ) ;
#19551=FACE_OUTER_BOUND ( 'NONE', #10086, .T. ) ;
#19620=CARTESIAN_POINT ( 'NONE',  ( 0.000000000000000000, -1.750000000000001554, 0.000000000000000000 ) ) ;
#19648=PLANE ( 'NONE',  #2814 ) ;
#19664=VERTEX_POINT ( 'NONE', #5216 ) ;
#19700=ORIENTED_EDGE ( 'NONE', *, *, #9642, .T. ) ;
#19749=EDGE_CURVE ( 'NONE', #5108, #19664, #16301, .T. ) ;
#19766=CARTESIAN_POINT ( 'NONE',  ( -0.4634555468559507507, -1.749999999999993561, -4.750000000000024869 ) ) ;
#19775=CARTESIAN_POINT ( 'NONE',  ( -3.997250504095343437, 1.750000000000008882, 2.576559036326544483 ) ) ;
#19797=CARTESIAN_POINT ( 'NONE',  ( 5.035458327682277080, -1.561572887838371226, -0.7783303370585006320 ) ) ;
#19800=CARTESIAN_POINT ( 'NONE',  ( 4.578118944855308570, 1.701165921963294858, 1.570465384416993349 ) ) ;
#19907=EDGE_CURVE ( 'NONE', #14175, #22294, #14467, .T. ) ;
#19982=DIRECTION ( 'NONE',  ( 0.8660254037844387076, 1.577721810442023611E-30, 0.5000000000000001110 ) ) ;
#20010=EDGE_LOOP ( 'NONE', ( #4160, #3795, #8903, #16635, #2065, #13187 ) ) ;
#20025=CIRCLE ( 'NONE', #10998, 4.750000000000000000 ) ;
#20064=ADVANCED_FACE ( 'NONE', ( #21432 ), #19648, .F. ) ;
#20071=ADVANCED_FACE ( 'NONE', ( #1761, #14347 ), #16213, .T. ) ;
#20097=ADVANCED_FACE ( 'NONE', ( #12221 ), #1323, .T. ) ;
#20151=ORIENTED_EDGE ( 'NONE', *, *, #1184, .T. ) ;
#20152=ORIENTED_EDGE ( 'NONE', *, *, #4941, .F. ) ;
#20169=CONICAL_SURFACE ( 'NONE', #4757, 4.750000000000000000, 1.047197551196600074 ) ;
#20172=CARTESIAN_POINT ( 'NONE',  ( 1.110223024625156540E-13, 1.749999999999998002, -4.750000000000000888 ) ) ;
#20177=CARTESIAN_POINT ( 'NONE',  ( 4.113620667976089607, -1.750000000000025757, 2.374999999999986677 ) ) ;
#20193=ORIENTED_EDGE ( 'NONE', *, *, #8520, .T. ) ;
#20235=EDGE_CURVE ( 'NONE', #16467, #13441, #17262, .T. ) ;
#20248=ORIENTED_EDGE ( 'NONE', *, *, #19324, .F. ) ;
#20352=EDGE_CURVE ( 'NONE', #22294, #14175, #580, .T. ) ;
#20364=DIRECTION ( 'NONE',  ( 8.438582421954110511E-32, 0.000000000000000000, 1.000000000000000000 ) ) ;
#20412=CIRCLE ( 'NONE', #1991, 4.750000000000000888 ) ;
#20428=EDGE_CURVE ( 'NONE', #22215, #8787, #483, .T. ) ;
#20458=CARTESIAN_POINT ( 'NONE',  ( -2.742413778650615086, 1.750000000000001554, -4.750000000000004441 ) ) ;
#20545=ORIENTED_EDGE ( 'NONE', *, *, #5437, .T. ) ;
#20566=ORIENTED_EDGE ( 'NONE', *, *, #1779, .F. ) ;
#20600=CARTESIAN_POINT ( 'NONE',  ( 1.110223024625156540E-13, -1.750000000000001554, -4.750000000000000888 ) ) ;
#20651=PRODUCT_DEFINITION_CONTEXT ( 'detailed design', #15079, 'design' ) ;
#20769=ORIENTED_EDGE ( 'NONE', *, *, #9253, .T. ) ;
#20775=AXIS2_PLACEMENT_3D ( 'NONE', #19469, #23131, #10638 ) ;
#20788=FACE_OUTER_BOUND ( 'NONE', #6305, .T. ) ;
#20850=CARTESIAN_POINT ( 'NONE',  ( -2.742413778650712342, 1.325747111984031834, 4.749999999999999112 ) ) ;
#20878=CARTESIAN_POINT ( 'NONE',  ( -2.296348136152782882, 1.454515171370275084, -4.750000000000025757 ) ) ;
#20953=PRODUCT_DEFINITION_SHAPE ( 'NONE', 'NONE',  #7617 ) ;
#21017=CARTESIAN_POINT ( 'NONE',  ( -4.113620667976089607, 1.749999999999998002, -2.375000000000029754 ) ) ;
#21029=EDGE_CURVE ( 'NONE', #6272, #9718, #4216, .T. ) ;
#21031=ORIENTED_EDGE ( 'NONE', *, *, #1184, .F. ) ;
#21044=PRODUCT_DEFINITION_FORMATION_WITH_SPECIFIED_SOURCE ( 'ANY', '', #13999, .NOT_KNOWN. ) ;
#21115=B_SPLINE_CURVE_WITH_KNOTS ( 'NONE', 3,
 ( #20600, #11407, #2471, #9650, #22240, #4466 ),
 .UNSPECIFIED., .F., .F.,
 ( 4, 2, 4 ),
 ( 0.007678960779285795915, 0.009067029725553659575, 0.01045509867182152497 ),
 .UNSPECIFIED. ) ;
#21136=ORIENTED_EDGE ( 'NONE', *, *, #9657, .F. ) ;
#21148=EDGE_LOOP ( 'NONE', ( #17653, #9951, #14936 ) ) ;
#21153=CARTESIAN_POINT ( 'NONE',  ( 0.9337610950194757953, -1.709055944985351960, 4.749999999999998224 ) ) ;
#21155=EDGE_CURVE ( 'NONE', #5108, #22294, #4565, .T. ) ;
#21163=DIRECTION ( 'NONE',  ( 0.000000000000000000, 1.000000000000000000, 0.000000000000000000 ) ) ;
#21190=CARTESIAN_POINT ( 'NONE',  ( 0.000000000000000000, 1.750000000000001554, 0.000000000000000000 ) ) ;
#21204=ORIENTED_EDGE ( 'NONE', *, *, #9157, .F. ) ;
#21221=CARTESIAN_POINT ( 'NONE',  ( -2.109645605488527628E-31, 1.750000000000001554, -2.500000000000000000 ) ) ;
#21231=CARTESIAN_POINT ( 'NONE',  ( 5.035458327682273527, 1.561572887838372337, 0.7783303370584975234 ) ) ;
#21255=CARTESIAN_POINT ( 'NONE',  ( 4.113620667976089607, -1.750000000000025757, 2.374999999999986677 ) ) ;
#21280=AXIS2_PLACEMENT_3D ( 'NONE', #20458, #19982, #3857 ) ;
#21294=CARTESIAN_POINT ( 'NONE',  ( 0.000000000000000000, 1.750000000000001554, 0.000000000000000000 ) ) ;
#21348=EDGE_CURVE ( 'NONE', #3913, #1642, #5071, .T. ) ;
#21360=ORIENTED_EDGE ( 'NONE', *, *, #9642, .F. ) ;
#21368=CARTESIAN_POINT ( 'NONE',  ( 0.000000000000000000, 1.750000000000001554, 0.000000000000000000 ) ) ;
#21408=DIRECTION ( 'NONE',  ( 8.438582421954109416E-32, 0.000000000000000000, 1.000000000000000000 ) ) ;
#21416=EDGE_LOOP ( 'NONE', ( #16466, #1327 ) ) ;
#21432=FACE_OUTER_BOUND ( 'NONE', #2352, .T. ) ;
#21465=ORIENTED_EDGE ( 'NONE', *, *, #18844, .F. ) ;
#21609=CARTESIAN_POINT ( 'NONE',  ( 0.000000000000000000, 1.750000000000001554, 0.000000000000000000 ) ) ;
#21613=ADVANCED_FACE ( 'NONE', ( #22670 ), #20169, .T. ) ;
#21636=DIRECTION ( 'NONE',  ( -8.438582421954109416E-32, 0.000000000000000000, -1.000000000000000000 ) ) ;
#21640=FACE_OUTER_BOUND ( 'NONE', #6448, .T. ) ;
#21680=DIRECTION ( 'NONE',  ( 0.000000000000000000, -1.000000000000000000, 0.000000000000000000 ) ) ;
#21726=VERTEX_POINT ( 'NONE', #20177 ) ;
#21744=VECTOR ( 'NONE', #12403, 1000.000000000000000 ) ;
#21825=CARTESIAN_POINT ( 'NONE',  ( 2.742413778650823364, 1.325747111984056037, -4.750000000000000888 ) ) ;
#21921=ORIENTED_EDGE ( 'NONE', *, *, #18898, .T. ) ;
#21962=AXIS2_PLACEMENT_3D ( 'NONE', #10353, #15528, #15642 ) ;
#21973=CARTESIAN_POINT ( 'NONE',  ( -5.035458327682192703, 1.561572887838423629, -0.7783303370584467862 ) ) ;
#22101=CARTESIAN_POINT ( 'NONE',  ( 2.742413778650823364, -1.325747111984059590, -4.750000000000000888 ) ) ;
#22115=AXIS2_PLACEMENT_3D ( 'NONE', #4943, #2963, #5306 ) ;
#22148=ORIENTED_EDGE ( 'NONE', *, *, #9269, .T. ) ;
#22182=ORIENTED_EDGE ( 'NONE', *, *, #14589, .F. ) ;
#22209=ORIENTED_EDGE ( 'NONE', *, *, #1878, .F. ) ;
#22215=VERTEX_POINT ( 'NONE', #18490 ) ;
#22240=CARTESIAN_POINT ( 'NONE',  ( 2.298974087852386550, -1.453757124409941204, -4.750000000000024869 ) ) ;
#22259=ORIENTED_EDGE ( 'NONE', *, *, #4332, .T. ) ;
#22267=CARTESIAN_POINT ( 'NONE',  ( -5.035458327682264645, -1.561572887838380108, 0.7783303370584921943 ) ) ;
#22294=VERTEX_POINT ( 'NONE', #1740 ) ;
#22376=ADVANCED_FACE ( 'NONE', ( #21640 ), #5515, .F. ) ;
#22403=CARTESIAN_POINT ( 'NONE',  ( -0.9238745060512566498, 1.710161125114598279, -4.750000000000025757 ) ) ;
#22461=CARTESIAN_POINT ( 'NONE',  ( 2.742413778650726108, 1.325747111984056037, 4.749999999999997335 ) ) ;
#22478=CYLINDRICAL_SURFACE ( 'NONE', #9597, 2.500000000000000000 ) ;
#22481=CARTESIAN_POINT ( 'NONE',  ( 2.966164998648759710, -1.454929939081820445, 4.362451518707887388 ) ) ;
#22518=STYLED_ITEM ( 'NONE', ( #16141 ), #3025 ) ;
#22520=CARTESIAN_POINT ( 'NONE',  ( -1.839530896101873925, 1.562503694756888439, -4.750000000000024869 ) ) ;
#22525=AXIS2_PLACEMENT_3D ( 'NONE', #16237, #21680, #19434 ) ;
#22594=FACE_OUTER_BOUND ( 'NONE', #17396, .T. ) ;
#22647=ORIENTED_EDGE ( 'NONE', *, *, #19324, .T. ) ;
#22670=FACE_OUTER_BOUND ( 'NONE', #2904, .T. ) ;
#22712=DIRECTION ( 'NONE',  ( 8.438582421954109416E-32, 0.000000000000000000, 1.000000000000000000 ) ) ;
#22713=VECTOR ( 'NONE', #17312, 1000.000000000000000 ) ;
#22737=B_SPLINE_CURVE_WITH_KNOTS ( 'NONE', 3,
 ( #19255, #1838, #8910, #21153, #10439, #8674 ),
 .UNSPECIFIED., .F., .F.,
 ( 4, 2, 4 ),
 ( 0.001997790223414142811, 0.003382245482991528586, 0.004766700742568914795 ),
 .UNSPECIFIED. ) ;
#22753=FACE_OUTER_BOUND ( 'NONE', #8492, .T. ) ;
#22762=EDGE_CURVE ( 'NONE', #21726, #23235, #6317, .T. ) ;
#22768=DIRECTION ( 'NONE',  ( 8.438582421954109416E-32, 0.000000000000000000, 1.000000000000000000 ) ) ;
#22835=EDGE_CURVE ( 'NONE', #16377, #13233, #4428, .T. ) ;
#22900=AXIS2_PLACEMENT_3D ( 'NONE', #23263, #8661, #8783 ) ;
#22922=DIRECTION ( 'NONE',  ( 0.000000000000000000, -1.000000000000000000, 0.000000000000000000 ) ) ;
#23049=CARTESIAN_POINT ( 'NONE',  ( 0.000000000000000000, -1.750000000000001554, 0.000000000000000000 ) ) ;
#23131=DIRECTION ( 'NONE',  ( 0.000000000000000000, -1.000000000000000000, 0.000000000000000000 ) ) ;
#23157=CARTESIAN_POINT ( 'NONE',  ( -2.742413778650712342, -1.325747111984083793, 4.749999999999999112 ) ) ;
#23235=VERTEX_POINT ( 'NONE', #11890 ) ;
#23255=SURFACE_STYLE_FILL_AREA ( #10986 ) ;
#23263=CARTESIAN_POINT ( 'NONE',  ( 0.000000000000000000, -1.750000000000001554, 0.000000000000000000 ) ) ;
ENDSEC;
END-ISO-10303-21;
